ISO-10303-21;
HEADER;
/* Generated by software containing ST-Developer
 * from STEP Tools, Inc. (www.steptools.com) 
 */

FILE_DESCRIPTION(
/* description */ ('Door-style hinge test fixture with detent'),
/* implementation_level */ '2;1');

FILE_NAME(
/* name */ 'Inner race spacer (1).step',
/* time_stamp */ '2026-10-28T03:24:57-07:00',
/* author */ (''),
/* organization */ (''),
/* preprocessor_version */ 'ST-DEVELOPER v20.2',
/* originating_system */ 'Autodesk Translation Framework v15.17.0.0',
/* authorisation */ '');

FILE_SCHEMA (('AUTOMOTIVE_DESIGN { 1 0 10303 214 3 1 1 }'));
ENDSEC;

DATA;
#10=MECHANICAL_DESIGN_GEOMETRIC_PRESENTATION_REPRESENTATION('',(#358),#9813);
#287=SHAPE_REPRESENTATION_RELATIONSHIP('SRR','None',#9966,#318);
#318=ADVANCED_BREP_SHAPE_REPRESENTATION('',(#396),#9809);
#358=STYLED_ITEM('',(#10183),#396);
#396=MANIFOLD_SOLID_BREP('Body1',#4791);
#493=FACE_BOUND('',#1301,.T.);
#494=FACE_BOUND('',#1303,.T.);
#646=PLANE('',#5696);
#647=PLANE('',#5697);
#919=FACE_OUTER_BOUND('',#1298,.T.);
#920=FACE_OUTER_BOUND('',#1299,.T.);
#921=FACE_OUTER_BOUND('',#1300,.T.);
#922=FACE_OUTER_BOUND('',#1302,.T.);
#1298=EDGE_LOOP('',(#4281,#4282,#4283,#4284));
#1299=EDGE_LOOP('',(#4285,#4286,#4287,#4288));
#1300=EDGE_LOOP('',(#4289));
#1301=EDGE_LOOP('',(#4290));
#1302=EDGE_LOOP('',(#4291));
#1303=EDGE_LOOP('',(#4292));
#1624=LINE('',#9623,#1944);
#1625=LINE('',#9629,#1945);
#1944=VECTOR('',#7149,0.505);
#1945=VECTOR('',#7156,0.7);
#2201=CIRCLE('',#5691,0.505);
#2202=CIRCLE('',#5692,0.505);
#2203=CIRCLE('',#5694,0.7);
#2204=CIRCLE('',#5695,0.7);
#2588=VERTEX_POINT('',#9620);
#2589=VERTEX_POINT('',#9622);
#2590=VERTEX_POINT('',#9626);
#2591=VERTEX_POINT('',#9628);
#3157=EDGE_CURVE('',#2588,#2588,#2201,.T.);
#3158=EDGE_CURVE('',#2588,#2589,#1624,.T.);
#3159=EDGE_CURVE('',#2589,#2589,#2202,.T.);
#3160=EDGE_CURVE('',#2590,#2590,#2203,.T.);
#3161=EDGE_CURVE('',#2590,#2591,#1625,.T.);
#3162=EDGE_CURVE('',#2591,#2591,#2204,.T.);
#4281=ORIENTED_EDGE('',*,*,#3157,.F.);
#4282=ORIENTED_EDGE('',*,*,#3158,.T.);
#4283=ORIENTED_EDGE('',*,*,#3159,.T.);
#4284=ORIENTED_EDGE('',*,*,#3158,.F.);
#4285=ORIENTED_EDGE('',*,*,#3160,.F.);
#4286=ORIENTED_EDGE('',*,*,#3161,.T.);
#4287=ORIENTED_EDGE('',*,*,#3162,.T.);
#4288=ORIENTED_EDGE('',*,*,#3161,.F.);
#4289=ORIENTED_EDGE('',*,*,#3160,.T.);
#4290=ORIENTED_EDGE('',*,*,#3157,.T.);
#4291=ORIENTED_EDGE('',*,*,#3162,.F.);
#4292=ORIENTED_EDGE('',*,*,#3159,.F.);
#4460=CYLINDRICAL_SURFACE('',#5690,0.505);
#4461=CYLINDRICAL_SURFACE('',#5693,0.7);
#4724=ADVANCED_FACE('',(#919),#4460,.F.);
#4725=ADVANCED_FACE('',(#920),#4461,.T.);
#4726=ADVANCED_FACE('',(#921,#493),#646,.T.);
#4727=ADVANCED_FACE('',(#922,#494),#647,.F.);
#4791=CLOSED_SHELL('',(#4724,#4725,#4726,#4727));
#5689=AXIS2_PLACEMENT_3D('',#9618,#7143,#7144);
#5690=AXIS2_PLACEMENT_3D('',#9619,#7145,#7146);
#5691=AXIS2_PLACEMENT_3D('',#9621,#7147,#7148);
#5692=AXIS2_PLACEMENT_3D('',#9624,#7150,#7151);
#5693=AXIS2_PLACEMENT_3D('',#9625,#7152,#7153);
#5694=AXIS2_PLACEMENT_3D('',#9627,#7154,#7155);
#5695=AXIS2_PLACEMENT_3D('',#9630,#7157,#7158);
#5696=AXIS2_PLACEMENT_3D('',#9631,#7159,#7160);
#5697=AXIS2_PLACEMENT_3D('',#9632,#7161,#7162);
#7143=DIRECTION('axis',(0.,0.,1.));
#7144=DIRECTION('refdir',(1.,0.,0.));
#7145=DIRECTION('center_axis',(0.,0.,1.));
#7146=DIRECTION('ref_axis',(1.,0.,0.));
#7147=DIRECTION('center_axis',(0.,0.,-1.));
#7148=DIRECTION('ref_axis',(1.,0.,0.));
#7149=DIRECTION('',(0.,0.,-1.));
#7150=DIRECTION('center_axis',(0.,0.,-1.));
#7151=DIRECTION('ref_axis',(1.,0.,0.));
#7152=DIRECTION('center_axis',(0.,0.,1.));
#7153=DIRECTION('ref_axis',(1.,0.,0.));
#7154=DIRECTION('center_axis',(0.,0.,1.));
#7155=DIRECTION('ref_axis',(1.,0.,0.));
#7156=DIRECTION('',(0.,0.,-1.));
#7157=DIRECTION('center_axis',(0.,0.,1.));
#7158=DIRECTION('ref_axis',(1.,0.,0.));
#7159=DIRECTION('center_axis',(0.,0.,1.));
#7160=DIRECTION('ref_axis',(1.,0.,0.));
#7161=DIRECTION('center_axis',(0.,0.,1.));
#7162=DIRECTION('ref_axis',(1.,0.,0.));
#9618=CARTESIAN_POINT('',(0.,0.,0.));
#9619=CARTESIAN_POINT('Origin',(0.,0.,10.));
#9620=CARTESIAN_POINT('',(-0.505,-6.18446633569413E-17,10.6));
#9621=CARTESIAN_POINT('Origin',(0.,0.,10.6));
#9622=CARTESIAN_POINT('',(-0.505,-6.18446633569413E-17,10.));
#9623=CARTESIAN_POINT('',(-0.505,-6.18446633569413E-17,10.));
#9624=CARTESIAN_POINT('Origin',(0.,0.,10.));
#9625=CARTESIAN_POINT('Origin',(0.,0.,10.));
#9626=CARTESIAN_POINT('',(-0.7,-8.57252759403147E-17,10.6));
#9627=CARTESIAN_POINT('Origin',(0.,0.,10.6));
#9628=CARTESIAN_POINT('',(-0.7,-8.57252759403147E-17,10.));
#9629=CARTESIAN_POINT('',(-0.7,-8.57252759403147E-17,10.));
#9630=CARTESIAN_POINT('Origin',(0.,0.,10.));
#9631=CARTESIAN_POINT('Origin',(0.,0.,10.6));
#9632=CARTESIAN_POINT('Origin',(0.,0.,10.));
#9773=UNCERTAINTY_MEASURE_WITH_UNIT(LENGTH_MEASURE(0.001),#9814,
'DISTANCE_ACCURACY_VALUE',
'Maximum model space distance between geometric entities at asserted c
onnectivities');
#9777=UNCERTAINTY_MEASURE_WITH_UNIT(LENGTH_MEASURE(0.001),#9814,
'DISTANCE_ACCURACY_VALUE',
'Maximum model space distance between geometric entities at asserted c
onnectivities');
#9809=(
GEOMETRIC_REPRESENTATION_CONTEXT(3)
GLOBAL_UNCERTAINTY_ASSIGNED_CONTEXT((#9773))
GLOBAL_UNIT_ASSIGNED_CONTEXT((#9814,#9816,#9817))
REPRESENTATION_CONTEXT('','3D')
);
#9813=(
GEOMETRIC_REPRESENTATION_CONTEXT(3)
GLOBAL_UNCERTAINTY_ASSIGNED_CONTEXT((#9777))
GLOBAL_UNIT_ASSIGNED_CONTEXT((#9814,#9816,#9817))
REPRESENTATION_CONTEXT('','3D')
);
#9814=(
LENGTH_UNIT()
NAMED_UNIT(*)
SI_UNIT(.CENTI.,.METRE.)
);
#9816=(
NAMED_UNIT(*)
PLANE_ANGLE_UNIT()
SI_UNIT($,.RADIAN.)
);
#9817=(
NAMED_UNIT(*)
SI_UNIT($,.STERADIAN.)
SOLID_ANGLE_UNIT()
);
#9849=SHAPE_DEFINITION_REPRESENTATION(#9922,#9966);
#9922=PRODUCT_DEFINITION_SHAPE('',$,#10002);
#9966=SHAPE_REPRESENTATION('',(#5689),#9809);
#9970=PRODUCT_DEFINITION_CONTEXT('part definition',#10077,'design');
#10002=PRODUCT_DEFINITION('Inner race spacer (1)','Inner race spacer (1)',
#10037,#9970);
#10037=PRODUCT_DEFINITION_FORMATION('',$,#10110);
#10077=APPLICATION_CONTEXT(
'Core Data for Automotive Mechanical Design Process');
#10078=PRODUCT_CONTEXT('part definition',#10077,'mechanical');
#10110=PRODUCT('Inner race spacer (1)','Inner race spacer (1)',
'Inner race spacer (1)',(#10078));
#10177=COLOUR_RGB('Grey',0.48,0.52,0.57);
#10178=FILL_AREA_STYLE_COLOUR('',#10177);
#10179=FILL_AREA_STYLE('',(#10178));
#10180=SURFACE_STYLE_FILL_AREA(#10179);
#10181=SURFACE_SIDE_STYLE('',(#10180));
#10182=SURFACE_STYLE_USAGE(.BOTH.,#10181);
#10183=PRESENTATION_STYLE_ASSIGNMENT((#10182));
ENDSEC;
END-ISO-10303-21;
